ISO-10303-21;
HEADER;
FILE_DESCRIPTION((''),'2;1');
FILE_NAME('Clamp_Bolt_4.step','2026-10-09T10:15:02-07:00',(''),(''),'','','');
FILE_SCHEMA (('AUTOMOTIVE_DESIGN { 1 0 10303 214 3 1 1 }'));
ENDSEC;
DATA;
#10=MECHANICAL_DESIGN_GEOMETRIC_PRESENTATION_REPRESENTATION('',(#92),#6779);
#57=TOROIDAL_SURFACE('',#4417,4.4,0.6) ;
#58=TOROIDAL_SURFACE('',#4421,3.25,0.25) ;
#72=SHAPE_REPRESENTATION_RELATIONSHIP('SRR','None',#6826,#82) ;
#82=ADVANCED_BREP_SHAPE_REPRESENTATION('',(#102),#6778) ;
#92=STYLED_ITEM('',(#6877),#102) ;
#102=MANIFOLD_SOLID_BREP('Body1',#3904) ;
#133=FACE_BOUND('',#838,.T.) ;
#134=FACE_BOUND('',#840,.T.) ;
#253=PLANE('',#4403) ;
#254=PLANE('',#4404) ;
#255=PLANE('',#4405) ;
#256=PLANE('',#4406) ;
#257=PLANE('',#4407) ;
#258=PLANE('',#4408) ;
#259=PLANE('',#4409) ;
#260=PLANE('',#4410) ;
#261=PLANE('',#4412) ;
#262=PLANE('',#4415) ;
#326=CONICAL_SURFACE('',#4426,2.5,0.785398163397) ;
#556=FACE_OUTER_BOUND('',#830,.T.) ;
#557=FACE_OUTER_BOUND('',#831,.T.) ;
#558=FACE_OUTER_BOUND('',#832,.T.) ;
#559=FACE_OUTER_BOUND('',#833,.T.) ;
#560=FACE_OUTER_BOUND('',#834,.T.) ;
#561=FACE_OUTER_BOUND('',#835,.T.) ;
#562=FACE_OUTER_BOUND('',#836,.T.) ;
#563=FACE_OUTER_BOUND('',#837,.T.) ;
#564=FACE_OUTER_BOUND('',#839,.T.) ;
#565=FACE_OUTER_BOUND('',#841,.T.) ;
#566=FACE_OUTER_BOUND('',#842,.T.) ;
#567=FACE_OUTER_BOUND('',#843,.T.) ;
#568=FACE_OUTER_BOUND('',#844,.T.) ;
#569=FACE_OUTER_BOUND('',#845,.T.) ;
#570=FACE_OUTER_BOUND('',#846,.T.) ;
#830=EDGE_LOOP('',(#3543,#3544,#3545,#3546)) ;
#831=EDGE_LOOP('',(#3547,#3548,#3549,#3550)) ;
#832=EDGE_LOOP('',(#3551,#3552,#3553,#3554)) ;
#833=EDGE_LOOP('',(#3555,#3556,#3557,#3558,#3559,#3560)) ;
#834=EDGE_LOOP('',(#3561,#3562,#3563,#3564)) ;
#835=EDGE_LOOP('',(#3565,#3566,#3567,#3568)) ;
#836=EDGE_LOOP('',(#3569,#3570,#3571,#3572)) ;
#837=EDGE_LOOP('',(#3573)) ;
#838=EDGE_LOOP('',(#3574,#3575,#3576,#3577,#3578,#3579)) ;
#839=EDGE_LOOP('',(#3580)) ;
#840=EDGE_LOOP('',(#3581)) ;
#841=EDGE_LOOP('',(#3582)) ;
#842=EDGE_LOOP('',(#3583,#3584,#3585,#3586)) ;
#843=EDGE_LOOP('',(#3587,#3588,#3589,#3590)) ;
#844=EDGE_LOOP('',(#3591,#3592,#3593,#3594)) ;
#845=EDGE_LOOP('',(#3595,#3596,#3597,#3598)) ;
#846=EDGE_LOOP('',(#3599,#3600,#3601,#3602)) ;
#1186=LINE('',#6685,#1546) ;
#1187=LINE('',#6687,#1547) ;
#1188=LINE('',#6689,#1548) ;
#1189=LINE('',#6690,#1549) ;
#1190=LINE('',#6694,#1550) ;
#1191=LINE('',#6695,#1551) ;
#1192=LINE('',#6696,#1552) ;
#1193=LINE('',#6699,#1553) ;
#1194=LINE('',#6701,#1554) ;
#1195=LINE('',#6702,#1555) ;
#1196=LINE('',#6705,#1556) ;
#1197=LINE('',#6707,#1557) ;
#1198=LINE('',#6708,#1558) ;
#1199=LINE('',#6711,#1559) ;
#1200=LINE('',#6712,#1560) ;
#1201=LINE('',#6715,#1561) ;
#1202=LINE('',#6716,#1562) ;
#1203=LINE('',#6718,#1563) ;
#1204=LINE('',#6735,#1564) ;
#1205=LINE('',#6742,#1565) ;
#1206=LINE('',#6745,#1566) ;
#1546=VECTOR('',#5552,1.) ;
#1547=VECTOR('',#5553,1.) ;
#1548=VECTOR('',#5554,1.) ;
#1549=VECTOR('',#5555,1.) ;
#1550=VECTOR('',#5558,1.) ;
#1551=VECTOR('',#5559,0.99999999999962) ;
#1552=VECTOR('',#5560,0.99999999999962) ;
#1553=VECTOR('',#5563,0.99999999999962) ;
#1554=VECTOR('',#5564,1.) ;
#1555=VECTOR('',#5565,0.99999999999962) ;
#1556=VECTOR('',#5568,0.99999999999962) ;
#1557=VECTOR('',#5569,1.) ;
#1558=VECTOR('',#5570,0.99999999999962) ;
#1559=VECTOR('',#5573,1.) ;
#1560=VECTOR('',#5574,0.99999999999962) ;
#1561=VECTOR('',#5577,0.99999999999962) ;
#1562=VECTOR('',#5578,1.) ;
#1563=VECTOR('',#5581,1.) ;
#1564=VECTOR('',#5604,5.) ;
#1565=VECTOR('',#5613,3.) ;
#1566=VECTOR('',#5618,2.5) ;
#1714=CIRCLE('',#4411,4.4) ;
#1715=CIRCLE('',#4413,5.) ;
#1716=CIRCLE('',#4414,3.25) ;
#1717=CIRCLE('',#4416,2.5) ;
#1718=CIRCLE('',#4418,0.6) ;
#1719=CIRCLE('',#4419,5.) ;
#1720=CIRCLE('',#4422,0.25) ;
#1721=CIRCLE('',#4423,3.) ;
#1722=CIRCLE('',#4425,3.) ;
#2012=VERTEX_POINT('',#6683) ;
#2013=VERTEX_POINT('',#6684) ;
#2014=VERTEX_POINT('',#6686) ;
#2015=VERTEX_POINT('',#6688) ;
#2016=VERTEX_POINT('',#6692) ;
#2017=VERTEX_POINT('',#6693) ;
#2018=VERTEX_POINT('',#6698) ;
#2019=VERTEX_POINT('',#6700) ;
#2020=VERTEX_POINT('',#6704) ;
#2021=VERTEX_POINT('',#6706) ;
#2022=VERTEX_POINT('',#6710) ;
#2023=VERTEX_POINT('',#6714) ;
#2024=VERTEX_POINT('',#6720) ;
#2025=VERTEX_POINT('',#6723) ;
#2026=VERTEX_POINT('',#6725) ;
#2027=VERTEX_POINT('',#6728) ;
#2028=VERTEX_POINT('',#6731) ;
#2029=VERTEX_POINT('',#6737) ;
#2030=VERTEX_POINT('',#6741) ;
#2525=EDGE_CURVE('',#2012,#2013,#1186,.T.) ;
#2526=EDGE_CURVE('',#2012,#2014,#1187,.T.) ;
#2527=EDGE_CURVE('',#2014,#2015,#1188,.T.) ;
#2528=EDGE_CURVE('',#2013,#2015,#1189,.T.) ;
#2529=EDGE_CURVE('',#2016,#2017,#1190,.T.) ;
#2530=EDGE_CURVE('',#2016,#2012,#1191,.T.) ;
#2531=EDGE_CURVE('',#2017,#2013,#1192,.T.) ;
#2532=EDGE_CURVE('',#2014,#2018,#1193,.T.) ;
#2533=EDGE_CURVE('',#2018,#2019,#1194,.T.) ;
#2534=EDGE_CURVE('',#2015,#2019,#1195,.T.) ;
#2535=EDGE_CURVE('',#2019,#2020,#1196,.T.) ;
#2536=EDGE_CURVE('',#2020,#2021,#1197,.T.) ;
#2537=EDGE_CURVE('',#2021,#2017,#1198,.T.) ;
#2538=EDGE_CURVE('',#2022,#2021,#1199,.T.) ;
#2539=EDGE_CURVE('',#2022,#2016,#1200,.T.) ;
#2540=EDGE_CURVE('',#2018,#2023,#1201,.T.) ;
#2541=EDGE_CURVE('',#2023,#2020,#1202,.T.) ;
#2542=EDGE_CURVE('',#2023,#2022,#1203,.T.) ;
#2543=EDGE_CURVE('',#2024,#2024,#1714,.T.) ;
#2544=EDGE_CURVE('',#2025,#2025,#1715,.T.) ;
#2545=EDGE_CURVE('',#2026,#2026,#1716,.T.) ;
#2546=EDGE_CURVE('',#2027,#2027,#1717,.T.) ;
#2547=EDGE_CURVE('',#2024,#2028,#1718,.T.) ;
#2548=EDGE_CURVE('',#2028,#2028,#1719,.T.) ;
#2549=EDGE_CURVE('',#2028,#2025,#1204,.T.) ;
#2550=EDGE_CURVE('',#2026,#2029,#1720,.T.) ;
#2551=EDGE_CURVE('',#2029,#2029,#1721,.T.) ;
#2552=EDGE_CURVE('',#2029,#2030,#1205,.T.) ;
#2553=EDGE_CURVE('',#2030,#2030,#1722,.T.) ;
#2554=EDGE_CURVE('',#2030,#2027,#1206,.T.) ;
#3543=ORIENTED_EDGE('',*,*,#2525,.F.) ;
#3544=ORIENTED_EDGE('',*,*,#2526,.T.) ;
#3545=ORIENTED_EDGE('',*,*,#2527,.T.) ;
#3546=ORIENTED_EDGE('',*,*,#2528,.F.) ;
#3547=ORIENTED_EDGE('',*,*,#2529,.F.) ;
#3548=ORIENTED_EDGE('',*,*,#2530,.T.) ;
#3549=ORIENTED_EDGE('',*,*,#2525,.T.) ;
#3550=ORIENTED_EDGE('',*,*,#2531,.F.) ;
#3551=ORIENTED_EDGE('',*,*,#2527,.F.) ;
#3552=ORIENTED_EDGE('',*,*,#2532,.T.) ;
#3553=ORIENTED_EDGE('',*,*,#2533,.T.) ;
#3554=ORIENTED_EDGE('',*,*,#2534,.F.) ;
#3555=ORIENTED_EDGE('',*,*,#2528,.T.) ;
#3556=ORIENTED_EDGE('',*,*,#2534,.T.) ;
#3557=ORIENTED_EDGE('',*,*,#2535,.T.) ;
#3558=ORIENTED_EDGE('',*,*,#2536,.T.) ;
#3559=ORIENTED_EDGE('',*,*,#2537,.T.) ;
#3560=ORIENTED_EDGE('',*,*,#2531,.T.) ;
#3561=ORIENTED_EDGE('',*,*,#2538,.F.) ;
#3562=ORIENTED_EDGE('',*,*,#2539,.T.) ;
#3563=ORIENTED_EDGE('',*,*,#2529,.T.) ;
#3564=ORIENTED_EDGE('',*,*,#2537,.F.) ;
#3565=ORIENTED_EDGE('',*,*,#2533,.F.) ;
#3566=ORIENTED_EDGE('',*,*,#2540,.T.) ;
#3567=ORIENTED_EDGE('',*,*,#2541,.T.) ;
#3568=ORIENTED_EDGE('',*,*,#2535,.F.) ;
#3569=ORIENTED_EDGE('',*,*,#2541,.F.) ;
#3570=ORIENTED_EDGE('',*,*,#2542,.T.) ;
#3571=ORIENTED_EDGE('',*,*,#2538,.T.) ;
#3572=ORIENTED_EDGE('',*,*,#2536,.F.) ;
#3573=ORIENTED_EDGE('',*,*,#2543,.T.) ;
#3574=ORIENTED_EDGE('',*,*,#2539,.F.) ;
#3575=ORIENTED_EDGE('',*,*,#2542,.F.) ;
#3576=ORIENTED_EDGE('',*,*,#2540,.F.) ;
#3577=ORIENTED_EDGE('',*,*,#2532,.F.) ;
#3578=ORIENTED_EDGE('',*,*,#2526,.F.) ;
#3579=ORIENTED_EDGE('',*,*,#2530,.F.) ;
#3580=ORIENTED_EDGE('',*,*,#2544,.F.) ;
#3581=ORIENTED_EDGE('',*,*,#2545,.T.) ;
#3582=ORIENTED_EDGE('',*,*,#2546,.F.) ;
#3583=ORIENTED_EDGE('',*,*,#2543,.F.) ;
#3584=ORIENTED_EDGE('',*,*,#2547,.T.) ;
#3585=ORIENTED_EDGE('',*,*,#2548,.T.) ;
#3586=ORIENTED_EDGE('',*,*,#2547,.F.) ;
#3587=ORIENTED_EDGE('',*,*,#2548,.F.) ;
#3588=ORIENTED_EDGE('',*,*,#2549,.T.) ;
#3589=ORIENTED_EDGE('',*,*,#2544,.T.) ;
#3590=ORIENTED_EDGE('',*,*,#2549,.F.) ;
#3591=ORIENTED_EDGE('',*,*,#2545,.F.) ;
#3592=ORIENTED_EDGE('',*,*,#2550,.T.) ;
#3593=ORIENTED_EDGE('',*,*,#2551,.T.) ;
#3594=ORIENTED_EDGE('',*,*,#2550,.F.) ;
#3595=ORIENTED_EDGE('',*,*,#2551,.F.) ;
#3596=ORIENTED_EDGE('',*,*,#2552,.T.) ;
#3597=ORIENTED_EDGE('',*,*,#2553,.T.) ;
#3598=ORIENTED_EDGE('',*,*,#2552,.F.) ;
#3599=ORIENTED_EDGE('',*,*,#2553,.F.) ;
#3600=ORIENTED_EDGE('',*,*,#2554,.T.) ;
#3601=ORIENTED_EDGE('',*,*,#2546,.T.) ;
#3602=ORIENTED_EDGE('',*,*,#2554,.F.) ;
#3649=CYLINDRICAL_SURFACE('',#4420,5.) ;
#3650=CYLINDRICAL_SURFACE('',#4424,3.) ;
#3880=ADVANCED_FACE('',(#556),#253,.T.) ;
#3881=ADVANCED_FACE('',(#557),#254,.T.) ;
#3882=ADVANCED_FACE('',(#558),#255,.T.) ;
#3883=ADVANCED_FACE('',(#559),#256,.T.) ;
#3884=ADVANCED_FACE('',(#560),#257,.T.) ;
#3885=ADVANCED_FACE('',(#561),#258,.T.) ;
#3886=ADVANCED_FACE('',(#562),#259,.T.) ;
#3887=ADVANCED_FACE('',(#563,#133),#260,.T.) ;
#3888=ADVANCED_FACE('',(#564,#134),#261,.F.) ;
#3889=ADVANCED_FACE('',(#565),#262,.F.) ;
#3890=ADVANCED_FACE('',(#566),#57,.T.) ;
#3891=ADVANCED_FACE('',(#567),#3649,.T.) ;
#3892=ADVANCED_FACE('',(#568),#58,.F.) ;
#3893=ADVANCED_FACE('',(#569),#3650,.T.) ;
#3894=ADVANCED_FACE('',(#570),#326,.T.) ;
#3904=CLOSED_SHELL('',(#3880,#3881,#3882,#3883,#3884,#3885,#3886,#3887,
#3888,#3889,#3890,#3891,#3892,#3893,#3894)) ;
#4402=AXIS2_PLACEMENT_3D('',#6681,#5548,#5549) ;
#4403=AXIS2_PLACEMENT_3D('',#6682,#5550,#5551) ;
#4404=AXIS2_PLACEMENT_3D('',#6691,#5556,#5557) ;
#4405=AXIS2_PLACEMENT_3D('',#6697,#5561,#5562) ;
#4406=AXIS2_PLACEMENT_3D('',#6703,#5566,#5567) ;
#4407=AXIS2_PLACEMENT_3D('',#6709,#5571,#5572) ;
#4408=AXIS2_PLACEMENT_3D('',#6713,#5575,#5576) ;
#4409=AXIS2_PLACEMENT_3D('',#6717,#5579,#5580) ;
#4410=AXIS2_PLACEMENT_3D('',#6719,#5582,#5583) ;
#4411=AXIS2_PLACEMENT_3D('',#6721,#5584,#5585) ;
#4412=AXIS2_PLACEMENT_3D('',#6722,#5586,#5587) ;
#4413=AXIS2_PLACEMENT_3D('',#6724,#5588,#5589) ;
#4414=AXIS2_PLACEMENT_3D('',#6726,#5590,#5591) ;
#4415=AXIS2_PLACEMENT_3D('',#6727,#5592,#5593) ;
#4416=AXIS2_PLACEMENT_3D('',#6729,#5594,#5595) ;
#4417=AXIS2_PLACEMENT_3D('',#6730,#5596,#5597) ;
#4418=AXIS2_PLACEMENT_3D('',#6732,#5598,#5599) ;
#4419=AXIS2_PLACEMENT_3D('',#6733,#5600,#5601) ;
#4420=AXIS2_PLACEMENT_3D('',#6734,#5602,#5603) ;
#4421=AXIS2_PLACEMENT_3D('',#6736,#5605,#5606) ;
#4422=AXIS2_PLACEMENT_3D('',#6738,#5607,#5608) ;
#4423=AXIS2_PLACEMENT_3D('',#6739,#5609,#5610) ;
#4424=AXIS2_PLACEMENT_3D('',#6740,#5611,#5612) ;
#4425=AXIS2_PLACEMENT_3D('',#6743,#5614,#5615) ;
#4426=AXIS2_PLACEMENT_3D('',#6744,#5616,#5617) ;
#5548=DIRECTION('axis',(0.,0.,1.)) ;
#5549=DIRECTION('refdir',(1.,0.,0.)) ;
#5550=DIRECTION('center_axis',(1.,0.,-1.53837014911E-16)) ;
#5551=DIRECTION('ref_axis',(-1.53837014911E-16,0.,-1.)) ;
#5552=DIRECTION('',(0.,1.,0.)) ;
#5553=DIRECTION('',(0.,0.,-1.)) ;
#5554=DIRECTION('',(0.,1.,0.)) ;
#5555=DIRECTION('',(0.,0.,-1.)) ;
#5556=DIRECTION('center_axis',(0.50000000000019,0.,-0.866025403784329)) ;
#5557=DIRECTION('ref_axis',(-0.866025403784329,0.,-0.50000000000019)) ;
#5558=DIRECTION('',(0.,1.,0.)) ;
#5559=DIRECTION('',(-0.866025403784329,0.,-0.50000000000019)) ;
#5560=DIRECTION('',(-0.866025403784329,0.,-0.50000000000019)) ;
#5561=DIRECTION('center_axis',(0.50000000000019,0.,0.866025403784329)) ;
#5562=DIRECTION('ref_axis',(0.866025403784329,0.,-0.50000000000019)) ;
#5563=DIRECTION('',(0.866025403784329,0.,-0.50000000000019)) ;
#5564=DIRECTION('',(0.,1.,0.)) ;
#5565=DIRECTION('',(0.866025403784329,0.,-0.50000000000019)) ;
#5566=DIRECTION('center_axis',(0.,-1.,0.)) ;
#5567=DIRECTION('ref_axis',(1.,0.,0.)) ;
#5568=DIRECTION('',(0.866025403784329,0.,0.50000000000019)) ;
#5569=DIRECTION('',(0.,0.,1.)) ;
#5570=DIRECTION('',(-0.866025403784329,0.,0.50000000000019)) ;
#5571=DIRECTION('center_axis',(-0.50000000000019,0.,-0.866025403784329)) ;
#5572=DIRECTION('ref_axis',(-0.866025403784329,0.,0.50000000000019)) ;
#5573=DIRECTION('',(0.,1.,0.)) ;
#5574=DIRECTION('',(-0.866025403784329,0.,0.50000000000019)) ;
#5575=DIRECTION('center_axis',(-0.50000000000019,0.,0.866025403784329)) ;
#5576=DIRECTION('ref_axis',(0.866025403784329,0.,0.50000000000019)) ;
#5577=DIRECTION('',(0.866025403784329,0.,0.50000000000019)) ;
#5578=DIRECTION('',(0.,1.,0.)) ;
#5579=DIRECTION('center_axis',(-1.,0.,0.)) ;
#5580=DIRECTION('ref_axis',(0.,0.,1.)) ;
#5581=DIRECTION('',(0.,0.,1.)) ;
#5582=DIRECTION('center_axis',(0.,-1.,0.)) ;
#5583=DIRECTION('ref_axis',(-1.,0.,0.)) ;
#5584=DIRECTION('center_axis',(0.,-1.,0.)) ;
#5585=DIRECTION('ref_axis',(0.,0.,1.)) ;
#5586=DIRECTION('center_axis',(0.,-1.,0.)) ;
#5587=DIRECTION('ref_axis',(-1.,0.,0.)) ;
#5588=DIRECTION('center_axis',(0.,-1.,0.)) ;
#5589=DIRECTION('ref_axis',(0.,0.,1.)) ;
#5590=DIRECTION('center_axis',(0.,-1.,0.)) ;
#5591=DIRECTION('ref_axis',(0.,0.,1.)) ;
#5592=DIRECTION('center_axis',(0.,-1.,0.)) ;
#5593=DIRECTION('ref_axis',(-1.,0.,0.)) ;
#5594=DIRECTION('center_axis',(0.,-1.,0.)) ;
#5595=DIRECTION('ref_axis',(0.,0.,1.)) ;
#5596=DIRECTION('center_axis',(0.,-1.,0.)) ;
#5597=DIRECTION('ref_axis',(0.479425538604205,0.,-0.877582561890372)) ;
#5598=DIRECTION('center_axis',(-0.877582561890372,0.,-0.479425538604205)) ;
#5599=DIRECTION('ref_axis',(-0.479425538604205,0.,0.877582561890372)) ;
#5600=DIRECTION('center_axis',(0.,-1.,0.)) ;
#5601=DIRECTION('ref_axis',(0.,0.,1.)) ;
#5602=DIRECTION('center_axis',(0.,-1.,0.)) ;
#5603=DIRECTION('ref_axis',(0.479425538604204,0.,-0.877582561890372)) ;
#5604=DIRECTION('',(0.,1.,0.)) ;
#5605=DIRECTION('center_axis',(0.,-1.,0.)) ;
#5606=DIRECTION('ref_axis',(0.479425538604204,0.,-0.877582561890372)) ;
#5607=DIRECTION('center_axis',(0.877582561890372,0.,0.479425538604204)) ;
#5608=DIRECTION('ref_axis',(-0.479425538604204,0.,0.877582561890372)) ;
#5609=DIRECTION('center_axis',(0.,-1.,0.)) ;
#5610=DIRECTION('ref_axis',(0.,0.,1.)) ;
#5611=DIRECTION('center_axis',(0.,-1.,0.)) ;
#5612=DIRECTION('ref_axis',(0.479425538604204,0.,-0.877582561890372)) ;
#5613=DIRECTION('',(0.,1.,0.)) ;
#5614=DIRECTION('center_axis',(0.,-1.,0.)) ;
#5615=DIRECTION('ref_axis',(0.,0.,1.)) ;
#5616=DIRECTION('center_axis',(0.,-1.,0.)) ;
#5617=DIRECTION('ref_axis',(0.479425538604204,0.,-0.877582561890372)) ;
#5618=DIRECTION('',(0.339005049420894,0.707106781186865,-0.620544580563467)) ;
#6681=CARTESIAN_POINT('',(0.,0.,0.)) ;
#6682=CARTESIAN_POINT('Origin',(32.5,-26.,-8.55662432703)) ;
#6683=CARTESIAN_POINT('',(32.5,-26.,-8.55662432703)) ;
#6684=CARTESIAN_POINT('',(32.5,-23.,-8.55662432703)) ;
#6685=CARTESIAN_POINT('',(32.5,-24.5,-8.55662432703)) ;
#6686=CARTESIAN_POINT('',(32.5,-26.,-11.443375673)) ;
#6687=CARTESIAN_POINT('',(32.5,-26.,-10.)) ;
#6688=CARTESIAN_POINT('',(32.5,-23.,-11.443375673)) ;
#6689=CARTESIAN_POINT('',(32.5,-24.5,-11.443375673)) ;
#6690=CARTESIAN_POINT('',(32.5,-23.,-10.)) ;
#6691=CARTESIAN_POINT('Origin',(35.,-26.,-7.11324865405)) ;
#6692=CARTESIAN_POINT('',(35.,-26.,-7.11324865405)) ;
#6693=CARTESIAN_POINT('',(35.,-23.,-7.11324865405)) ;
#6694=CARTESIAN_POINT('',(35.,-24.5,-7.11324865405)) ;
#6695=CARTESIAN_POINT('',(33.75,-26.,-7.83493649054)) ;
#6696=CARTESIAN_POINT('',(33.75,-23.,-7.83493649054)) ;
#6697=CARTESIAN_POINT('Origin',(32.5,-26.,-11.443375673)) ;
#6698=CARTESIAN_POINT('',(35.,-26.,-12.8867513459)) ;
#6699=CARTESIAN_POINT('',(33.75,-26.,-12.1650635095)) ;
#6700=CARTESIAN_POINT('',(35.,-23.,-12.8867513459)) ;
#6701=CARTESIAN_POINT('',(35.,-24.5,-12.8867513459)) ;
#6702=CARTESIAN_POINT('',(33.75,-23.,-12.1650635095)) ;
#6703=CARTESIAN_POINT('Origin',(-35.,-23.,10.)) ;
#6704=CARTESIAN_POINT('',(37.5,-23.,-11.443375673)) ;
#6705=CARTESIAN_POINT('',(36.25,-23.,-12.1650635095)) ;
#6706=CARTESIAN_POINT('',(37.5,-23.,-8.55662432703)) ;
#6707=CARTESIAN_POINT('',(37.5,-23.,-10.)) ;
#6708=CARTESIAN_POINT('',(36.25,-23.,-7.83493649054)) ;
#6709=CARTESIAN_POINT('Origin',(37.5,-26.,-8.55662432703)) ;
#6710=CARTESIAN_POINT('',(37.5,-26.,-8.55662432703)) ;
#6711=CARTESIAN_POINT('',(37.5,-24.5,-8.55662432703)) ;
#6712=CARTESIAN_POINT('',(36.25,-26.,-7.83493649054)) ;
#6713=CARTESIAN_POINT('Origin',(35.,-26.,-12.8867513459)) ;
#6714=CARTESIAN_POINT('',(37.5,-26.,-11.443375673)) ;
#6715=CARTESIAN_POINT('',(36.25,-26.,-12.1650635095)) ;
#6716=CARTESIAN_POINT('',(37.5,-24.5,-11.443375673)) ;
#6717=CARTESIAN_POINT('Origin',(37.5,-26.,-11.443375673)) ;
#6718=CARTESIAN_POINT('',(37.5,-26.,-10.)) ;
#6719=CARTESIAN_POINT('Origin',(-35.,-26.,10.)) ;
#6720=CARTESIAN_POINT('',(32.8905276301,-26.,-6.13863672768)) ;
#6721=CARTESIAN_POINT('Origin',(35.,-26.,-10.)) ;
#6722=CARTESIAN_POINT('Origin',(-35.,-20.,5.)) ;
#6723=CARTESIAN_POINT('',(32.602872307,-20.,-5.61208719055)) ;
#6724=CARTESIAN_POINT('Origin',(35.,-20.,-10.)) ;
#6725=CARTESIAN_POINT('',(33.4418669995,-20.,-7.14785667386)) ;
#6726=CARTESIAN_POINT('Origin',(35.,-20.,-10.)) ;
#6727=CARTESIAN_POINT('Origin',(-35.,40.,7.5)) ;
#6728=CARTESIAN_POINT('',(33.8014361535,40.,-7.80604359527)) ;
#6729=CARTESIAN_POINT('Origin',(35.,40.,-10.)) ;
#6730=CARTESIAN_POINT('Origin',(35.,-25.4,-10.)) ;
#6731=CARTESIAN_POINT('',(32.602872307,-25.4,-5.61208719055)) ;
#6732=CARTESIAN_POINT('Origin',(32.8905276301415,-25.4,-6.13863672768236)) ;
#6733=CARTESIAN_POINT('Origin',(35.,-25.4,-10.)) ;
#6734=CARTESIAN_POINT('Origin',(35.,7.,-10.)) ;
#6735=CARTESIAN_POINT('',(32.602872306979,7.,-5.61208719054814)) ;
#6736=CARTESIAN_POINT('Origin',(35.,-19.75,-10.)) ;
#6737=CARTESIAN_POINT('',(33.5617233842,-19.75,-7.36725231433)) ;
#6738=CARTESIAN_POINT('Origin',(33.4418669995363,-19.75,-7.14785667385629)) ;
#6739=CARTESIAN_POINT('Origin',(35.,-19.75,-10.)) ;
#6740=CARTESIAN_POINT('Origin',(35.,7.,-10.)) ;
#6741=CARTESIAN_POINT('',(33.5617233842,39.5,-7.36725231433)) ;
#6742=CARTESIAN_POINT('',(33.5617233841874,7.,-7.36725231432888)) ;
#6743=CARTESIAN_POINT('Origin',(35.,39.5,-10.)) ;
#6744=CARTESIAN_POINT('Origin',(35.,40.,-10.)) ;
#6745=CARTESIAN_POINT('',(33.8014361534895,40.,-7.80604359527407)) ;
#6766=UNCERTAINTY_MEASURE_WITH_UNIT(LENGTH_MEASURE(0.01),#6780,
'DISTANCE_ACCURACY_VALUE',
'Maximum model space distance between geometric entities at asserted c
onnectivities') ;
#6767=UNCERTAINTY_MEASURE_WITH_UNIT(LENGTH_MEASURE(0.01),#6780,
'DISTANCE_ACCURACY_VALUE',
'Maximum model space distance between geometric entities at asserted c
onnectivities') ;
#6778=(
GEOMETRIC_REPRESENTATION_CONTEXT(3)
GLOBAL_UNCERTAINTY_ASSIGNED_CONTEXT((#6766))
GLOBAL_UNIT_ASSIGNED_CONTEXT((#6780,#6782,#6783))
REPRESENTATION_CONTEXT('','3D')
) ;
#6779=(
GEOMETRIC_REPRESENTATION_CONTEXT(3)
GLOBAL_UNCERTAINTY_ASSIGNED_CONTEXT((#6767))
GLOBAL_UNIT_ASSIGNED_CONTEXT((#6780,#6782,#6783))
REPRESENTATION_CONTEXT('','3D')
) ;
#6780=(
LENGTH_UNIT()
NAMED_UNIT(*)
SI_UNIT(.MILLI.,.METRE.)
) ;
#6782=(
NAMED_UNIT(*)
PLANE_ANGLE_UNIT()
SI_UNIT($,.RADIAN.)
) ;
#6783=(
NAMED_UNIT(*)
SI_UNIT($,.STERADIAN.)
SOLID_ANGLE_UNIT()
) ;
#6794=SHAPE_DEFINITION_REPRESENTATION(#6805,#6826) ;
#6805=PRODUCT_DEFINITION_SHAPE('',$,#6838) ;
#6826=SHAPE_REPRESENTATION('',(#4402),#6778) ;
#6827=PRODUCT_DEFINITION_CONTEXT('part definition',#6862,'design') ;
#6838=PRODUCT_DEFINITION('Clamp_Bolt_4','Clamp_Bolt_4',#6849,#6827) ;
#6849=PRODUCT_DEFINITION_FORMATION('',$,#6874) ;
#6862=APPLICATION_CONTEXT(
'Core Data for Automotive Mechanical Design Process') ;
#6863=PRODUCT_CONTEXT('part definition',#6862,'mechanical') ;
#6874=PRODUCT('Clamp_Bolt_4','Clamp_Bolt_4',$,(#6863)) ;
#6877=PRESENTATION_STYLE_ASSIGNMENT((#6880)) ;
#6880=SURFACE_STYLE_USAGE(.BOTH.,#6883) ;
#6883=SURFACE_SIDE_STYLE('',(#6886)) ;
#6886=SURFACE_STYLE_FILL_AREA(#6889) ;
#6889=FILL_AREA_STYLE('Opaque(203,203,203)',(#6892)) ;
#6892=FILL_AREA_STYLE_COLOUR('Opaque(203,203,203)',#6895) ;
#6895=COLOUR_RGB('Opaque(203,203,203)', 0.31764706, 0.68627451, 0.89019608) ;
ENDSEC;
END-ISO-10303-21;
